ISO-10303-21;
HEADER;
/* Generated by software containing ST-Developer
 * from STEP Tools, Inc. (www.steptools.com) 
 */

FILE_DESCRIPTION(
/* description */ (''),
/* implementation_level */ '2;1');

FILE_NAME(
/* name */ '11_Front_Bearing_6006.step',
/* time_stamp */ '2026-10-26T07:49:00-07:00',
/* author */ (''),
/* organization */ (''),
/* preprocessor_version */ 'ST-DEVELOPER v20.2',
/* originating_system */ 'Autodesk Translation Framework v15.15.0.0',
/* authorisation */ '');

FILE_SCHEMA (('AUTOMOTIVE_DESIGN { 1 0 10303 214 3 1 1 }'));
ENDSEC;

DATA;
#10=MECHANICAL_DESIGN_GEOMETRIC_PRESENTATION_REPRESENTATION('',(#184),#38507);
#154=SHAPE_REPRESENTATION_RELATIONSHIP('SRR','None',#38582,#169);
#169=ADVANCED_BREP_SHAPE_REPRESENTATION('',(#199),#38499);
#184=STYLED_ITEM('',(#38720),#199);
#199=MANIFOLD_SOLID_BREP('Body1',#15078);
#491=FACE_BOUND('',#3094,.T.);
#492=FACE_BOUND('',#3097,.T.);
#493=FACE_BOUND('',#3102,.T.);
#494=FACE_BOUND('',#3105,.T.);
#495=FACE_BOUND('',#3108,.T.);
#496=FACE_BOUND('',#3113,.T.);
#786=PLANE('',#16175);
#787=PLANE('',#16179);
#788=PLANE('',#16187);
#789=PLANE('',#16191);
#790=PLANE('',#16195);
#791=PLANE('',#16203);
#1494=CYLINDRICAL_SURFACE('',#16183,27.5);
#1495=CYLINDRICAL_SURFACE('',#16199,15.);
#2131=FACE_OUTER_BOUND('',#3092,.T.);
#2132=FACE_OUTER_BOUND('',#3093,.T.);
#2133=FACE_OUTER_BOUND('',#3095,.T.);
#2134=FACE_OUTER_BOUND('',#3096,.T.);
#2135=FACE_OUTER_BOUND('',#3098,.T.);
#2136=FACE_OUTER_BOUND('',#3099,.T.);
#2137=FACE_OUTER_BOUND('',#3100,.T.);
#2138=FACE_OUTER_BOUND('',#3101,.T.);
#2139=FACE_OUTER_BOUND('',#3103,.T.);
#2140=FACE_OUTER_BOUND('',#3104,.T.);
#2141=FACE_OUTER_BOUND('',#3106,.T.);
#2142=FACE_OUTER_BOUND('',#3107,.T.);
#2143=FACE_OUTER_BOUND('',#3109,.T.);
#2144=FACE_OUTER_BOUND('',#3110,.T.);
#2145=FACE_OUTER_BOUND('',#3111,.T.);
#2146=FACE_OUTER_BOUND('',#3112,.T.);
#3092=EDGE_LOOP('',(#12357,#12358,#12359,#12360));
#3093=EDGE_LOOP('',(#12361));
#3094=EDGE_LOOP('',(#12362));
#3095=EDGE_LOOP('',(#12363,#12364,#12365,#12366));
#3096=EDGE_LOOP('',(#12367));
#3097=EDGE_LOOP('',(#12368));
#3098=EDGE_LOOP('',(#12369,#12370,#12371,#12372));
#3099=EDGE_LOOP('',(#12373,#12374,#12375,#12376));
#3100=EDGE_LOOP('',(#12377,#12378,#12379,#12380));
#3101=EDGE_LOOP('',(#12381));
#3102=EDGE_LOOP('',(#12382));
#3103=EDGE_LOOP('',(#12383,#12384,#12385,#12386));
#3104=EDGE_LOOP('',(#12387));
#3105=EDGE_LOOP('',(#12388));
#3106=EDGE_LOOP('',(#12389,#12390,#12391,#12392));
#3107=EDGE_LOOP('',(#12393));
#3108=EDGE_LOOP('',(#12394));
#3109=EDGE_LOOP('',(#12395,#12396,#12397,#12398));
#3110=EDGE_LOOP('',(#12399,#12400,#12401,#12402));
#3111=EDGE_LOOP('',(#12403,#12404,#12405,#12406));
#3112=EDGE_LOOP('',(#12407));
#3113=EDGE_LOOP('',(#12408));
#4106=LINE('',#26850,#5175);
#4107=LINE('',#26857,#5176);
#4108=LINE('',#26865,#5177);
#4109=LINE('',#26869,#5178);
#4110=LINE('',#26873,#5179);
#4111=LINE('',#26879,#5180);
#4112=LINE('',#26887,#5181);
#4113=LINE('',#26893,#5182);
#4114=LINE('',#26897,#5183);
#4115=LINE('',#26901,#5184);
#5175=VECTOR('',#19193,19.15);
#5176=VECTOR('',#19202,23.9);
#5177=VECTOR('',#19213,27.3);
#5178=VECTOR('',#19218,27.5);
#5179=VECTOR('',#19223,27.3);
#5180=VECTOR('',#19230,23.9);
#5181=VECTOR('',#19241,19.15);
#5182=VECTOR('',#19248,15.2);
#5183=VECTOR('',#19253,15.);
#5184=VECTOR('',#19258,15.2);
#6073=CIRCLE('',#16173,19.3);
#6074=CIRCLE('',#16174,19.);
#6075=CIRCLE('',#16176,23.8);
#6076=CIRCLE('',#16178,24.);
#6077=CIRCLE('',#16180,27.1);
#6078=CIRCLE('',#16182,27.5);
#6079=CIRCLE('',#16184,27.5);
#6080=CIRCLE('',#16186,27.1);
#6081=CIRCLE('',#16188,24.);
#6082=CIRCLE('',#16190,23.8);
#6083=CIRCLE('',#16192,19.3);
#6084=CIRCLE('',#16194,19.);
#6085=CIRCLE('',#16196,15.4);
#6086=CIRCLE('',#16198,15.);
#6087=CIRCLE('',#16200,15.);
#6088=CIRCLE('',#16202,15.4);
#7078=VERTEX_POINT('',#26847);
#7079=VERTEX_POINT('',#26849);
#7080=VERTEX_POINT('',#26853);
#7081=VERTEX_POINT('',#26856);
#7082=VERTEX_POINT('',#26860);
#7083=VERTEX_POINT('',#26863);
#7084=VERTEX_POINT('',#26867);
#7085=VERTEX_POINT('',#26871);
#7086=VERTEX_POINT('',#26875);
#7087=VERTEX_POINT('',#26878);
#7088=VERTEX_POINT('',#26882);
#7089=VERTEX_POINT('',#26885);
#7090=VERTEX_POINT('',#26889);
#7091=VERTEX_POINT('',#26892);
#7092=VERTEX_POINT('',#26896);
#7093=VERTEX_POINT('',#26900);
#8927=EDGE_CURVE('',#7078,#7078,#6073,.T.);
#8928=EDGE_CURVE('',#7078,#7079,#4106,.T.);
#8929=EDGE_CURVE('',#7079,#7079,#6074,.T.);
#8930=EDGE_CURVE('',#7080,#7080,#6075,.T.);
#8931=EDGE_CURVE('',#7080,#7081,#4107,.T.);
#8932=EDGE_CURVE('',#7081,#7081,#6076,.T.);
#8933=EDGE_CURVE('',#7082,#7082,#6077,.T.);
#8934=EDGE_CURVE('',#7083,#7083,#6078,.T.);
#8935=EDGE_CURVE('',#7083,#7082,#4108,.T.);
#8936=EDGE_CURVE('',#7084,#7084,#6079,.T.);
#8937=EDGE_CURVE('',#7084,#7083,#4109,.T.);
#8938=EDGE_CURVE('',#7085,#7085,#6080,.T.);
#8939=EDGE_CURVE('',#7085,#7084,#4110,.T.);
#8940=EDGE_CURVE('',#7086,#7086,#6081,.T.);
#8941=EDGE_CURVE('',#7086,#7087,#4111,.T.);
#8942=EDGE_CURVE('',#7087,#7087,#6082,.T.);
#8943=EDGE_CURVE('',#7088,#7088,#6083,.T.);
#8944=EDGE_CURVE('',#7089,#7089,#6084,.T.);
#8945=EDGE_CURVE('',#7089,#7088,#4112,.T.);
#8946=EDGE_CURVE('',#7090,#7090,#6085,.T.);
#8947=EDGE_CURVE('',#7090,#7091,#4113,.T.);
#8948=EDGE_CURVE('',#7091,#7091,#6086,.T.);
#8949=EDGE_CURVE('',#7091,#7092,#4114,.T.);
#8950=EDGE_CURVE('',#7092,#7092,#6087,.T.);
#8951=EDGE_CURVE('',#7092,#7093,#4115,.T.);
#8952=EDGE_CURVE('',#7093,#7093,#6088,.T.);
#12357=ORIENTED_EDGE('',*,*,#8927,.F.);
#12358=ORIENTED_EDGE('',*,*,#8928,.T.);
#12359=ORIENTED_EDGE('',*,*,#8929,.T.);
#12360=ORIENTED_EDGE('',*,*,#8928,.F.);
#12361=ORIENTED_EDGE('',*,*,#8930,.F.);
#12362=ORIENTED_EDGE('',*,*,#8927,.T.);
#12363=ORIENTED_EDGE('',*,*,#8930,.T.);
#12364=ORIENTED_EDGE('',*,*,#8931,.T.);
#12365=ORIENTED_EDGE('',*,*,#8932,.F.);
#12366=ORIENTED_EDGE('',*,*,#8931,.F.);
#12367=ORIENTED_EDGE('',*,*,#8933,.F.);
#12368=ORIENTED_EDGE('',*,*,#8932,.T.);
#12369=ORIENTED_EDGE('',*,*,#8934,.F.);
#12370=ORIENTED_EDGE('',*,*,#8935,.T.);
#12371=ORIENTED_EDGE('',*,*,#8933,.T.);
#12372=ORIENTED_EDGE('',*,*,#8935,.F.);
#12373=ORIENTED_EDGE('',*,*,#8936,.F.);
#12374=ORIENTED_EDGE('',*,*,#8937,.T.);
#12375=ORIENTED_EDGE('',*,*,#8934,.T.);
#12376=ORIENTED_EDGE('',*,*,#8937,.F.);
#12377=ORIENTED_EDGE('',*,*,#8938,.F.);
#12378=ORIENTED_EDGE('',*,*,#8939,.T.);
#12379=ORIENTED_EDGE('',*,*,#8936,.T.);
#12380=ORIENTED_EDGE('',*,*,#8939,.F.);
#12381=ORIENTED_EDGE('',*,*,#8938,.T.);
#12382=ORIENTED_EDGE('',*,*,#8940,.F.);
#12383=ORIENTED_EDGE('',*,*,#8940,.T.);
#12384=ORIENTED_EDGE('',*,*,#8941,.T.);
#12385=ORIENTED_EDGE('',*,*,#8942,.F.);
#12386=ORIENTED_EDGE('',*,*,#8941,.F.);
#12387=ORIENTED_EDGE('',*,*,#8942,.T.);
#12388=ORIENTED_EDGE('',*,*,#8943,.F.);
#12389=ORIENTED_EDGE('',*,*,#8944,.F.);
#12390=ORIENTED_EDGE('',*,*,#8945,.T.);
#12391=ORIENTED_EDGE('',*,*,#8943,.T.);
#12392=ORIENTED_EDGE('',*,*,#8945,.F.);
#12393=ORIENTED_EDGE('',*,*,#8944,.T.);
#12394=ORIENTED_EDGE('',*,*,#8946,.F.);
#12395=ORIENTED_EDGE('',*,*,#8946,.T.);
#12396=ORIENTED_EDGE('',*,*,#8947,.T.);
#12397=ORIENTED_EDGE('',*,*,#8948,.F.);
#12398=ORIENTED_EDGE('',*,*,#8947,.F.);
#12399=ORIENTED_EDGE('',*,*,#8948,.T.);
#12400=ORIENTED_EDGE('',*,*,#8949,.T.);
#12401=ORIENTED_EDGE('',*,*,#8950,.F.);
#12402=ORIENTED_EDGE('',*,*,#8949,.F.);
#12403=ORIENTED_EDGE('',*,*,#8950,.T.);
#12404=ORIENTED_EDGE('',*,*,#8951,.T.);
#12405=ORIENTED_EDGE('',*,*,#8952,.F.);
#12406=ORIENTED_EDGE('',*,*,#8951,.F.);
#12407=ORIENTED_EDGE('',*,*,#8929,.F.);
#12408=ORIENTED_EDGE('',*,*,#8952,.T.);
#14163=CONICAL_SURFACE('',#16172,19.15,0.404891786285086);
#14164=CONICAL_SURFACE('',#16177,23.9,0.278299659005112);
#14165=CONICAL_SURFACE('',#16181,27.3,0.785398163397449);
#14166=CONICAL_SURFACE('',#16185,27.3,0.785398163397448);
#14167=CONICAL_SURFACE('',#16189,23.9,0.278299659005111);
#14168=CONICAL_SURFACE('',#16193,19.15,0.404891786285086);
#14169=CONICAL_SURFACE('',#16197,15.2,0.785398163397448);
#14170=CONICAL_SURFACE('',#16201,15.2,0.785398163397449);
#14698=ADVANCED_FACE('',(#2131),#14163,.T.);
#14699=ADVANCED_FACE('',(#2132,#491),#786,.T.);
#14700=ADVANCED_FACE('',(#2133),#14164,.F.);
#14701=ADVANCED_FACE('',(#2134,#492),#787,.T.);
#14702=ADVANCED_FACE('',(#2135),#14165,.T.);
#14703=ADVANCED_FACE('',(#2136),#1494,.T.);
#14704=ADVANCED_FACE('',(#2137),#14166,.T.);
#14705=ADVANCED_FACE('',(#2138,#493),#788,.T.);
#14706=ADVANCED_FACE('',(#2139),#14167,.F.);
#14707=ADVANCED_FACE('',(#2140,#494),#789,.T.);
#14708=ADVANCED_FACE('',(#2141),#14168,.T.);
#14709=ADVANCED_FACE('',(#2142,#495),#790,.T.);
#14710=ADVANCED_FACE('',(#2143),#14169,.F.);
#14711=ADVANCED_FACE('',(#2144),#1495,.F.);
#14712=ADVANCED_FACE('',(#2145),#14170,.F.);
#14713=ADVANCED_FACE('',(#2146,#496),#791,.T.);
#15078=CLOSED_SHELL('',(#14698,#14699,#14700,#14701,#14702,#14703,#14704,
#14705,#14706,#14707,#14708,#14709,#14710,#14711,#14712,#14713));
#16171=AXIS2_PLACEMENT_3D('',#26845,#19187,#19188);
#16172=AXIS2_PLACEMENT_3D('',#26846,#19189,#19190);
#16173=AXIS2_PLACEMENT_3D('',#26848,#19191,#19192);
#16174=AXIS2_PLACEMENT_3D('',#26851,#19194,#19195);
#16175=AXIS2_PLACEMENT_3D('',#26852,#19196,#19197);
#16176=AXIS2_PLACEMENT_3D('',#26854,#19198,#19199);
#16177=AXIS2_PLACEMENT_3D('',#26855,#19200,#19201);
#16178=AXIS2_PLACEMENT_3D('',#26858,#19203,#19204);
#16179=AXIS2_PLACEMENT_3D('',#26859,#19205,#19206);
#16180=AXIS2_PLACEMENT_3D('',#26861,#19207,#19208);
#16181=AXIS2_PLACEMENT_3D('',#26862,#19209,#19210);
#16182=AXIS2_PLACEMENT_3D('',#26864,#19211,#19212);
#16183=AXIS2_PLACEMENT_3D('',#26866,#19214,#19215);
#16184=AXIS2_PLACEMENT_3D('',#26868,#19216,#19217);
#16185=AXIS2_PLACEMENT_3D('',#26870,#19219,#19220);
#16186=AXIS2_PLACEMENT_3D('',#26872,#19221,#19222);
#16187=AXIS2_PLACEMENT_3D('',#26874,#19224,#19225);
#16188=AXIS2_PLACEMENT_3D('',#26876,#19226,#19227);
#16189=AXIS2_PLACEMENT_3D('',#26877,#19228,#19229);
#16190=AXIS2_PLACEMENT_3D('',#26880,#19231,#19232);
#16191=AXIS2_PLACEMENT_3D('',#26881,#19233,#19234);
#16192=AXIS2_PLACEMENT_3D('',#26883,#19235,#19236);
#16193=AXIS2_PLACEMENT_3D('',#26884,#19237,#19238);
#16194=AXIS2_PLACEMENT_3D('',#26886,#19239,#19240);
#16195=AXIS2_PLACEMENT_3D('',#26888,#19242,#19243);
#16196=AXIS2_PLACEMENT_3D('',#26890,#19244,#19245);
#16197=AXIS2_PLACEMENT_3D('',#26891,#19246,#19247);
#16198=AXIS2_PLACEMENT_3D('',#26894,#19249,#19250);
#16199=AXIS2_PLACEMENT_3D('',#26895,#19251,#19252);
#16200=AXIS2_PLACEMENT_3D('',#26898,#19254,#19255);
#16201=AXIS2_PLACEMENT_3D('',#26899,#19256,#19257);
#16202=AXIS2_PLACEMENT_3D('',#26902,#19259,#19260);
#16203=AXIS2_PLACEMENT_3D('',#26903,#19261,#19262);
#19187=DIRECTION('axis',(0.,0.,1.));
#19188=DIRECTION('refdir',(1.,0.,0.));
#19189=DIRECTION('center_axis',(1.,0.,0.));
#19190=DIRECTION('ref_axis',(0.,1.,0.));
#19191=DIRECTION('center_axis',(1.,0.,0.));
#19192=DIRECTION('ref_axis',(0.,0.,-1.));
#19193=DIRECTION('',(-0.919145030018057,0.39391929857917,4.82412008127352E-17));
#19194=DIRECTION('center_axis',(1.,0.,0.));
#19195=DIRECTION('ref_axis',(0.,0.,-1.));
#19196=DIRECTION('center_axis',(-1.,0.,0.));
#19197=DIRECTION('ref_axis',(0.,0.,1.));
#19198=DIRECTION('center_axis',(1.,0.,0.));
#19199=DIRECTION('ref_axis',(0.,0.,-1.));
#19200=DIRECTION('center_axis',(-1.,0.,0.));
#19201=DIRECTION('ref_axis',(0.,1.,0.));
#19202=DIRECTION('',(-0.961523947640823,-0.274721127897378,-3.36436349937675E-17));
#19203=DIRECTION('center_axis',(1.,0.,0.));
#19204=DIRECTION('ref_axis',(0.,0.,-1.));
#19205=DIRECTION('center_axis',(-1.,0.,0.));
#19206=DIRECTION('ref_axis',(0.,0.,1.));
#19207=DIRECTION('center_axis',(1.,0.,0.));
#19208=DIRECTION('ref_axis',(0.,0.,-1.));
#19209=DIRECTION('center_axis',(1.,0.,0.));
#19210=DIRECTION('ref_axis',(0.,1.,0.));
#19211=DIRECTION('center_axis',(1.,0.,0.));
#19212=DIRECTION('ref_axis',(0.,0.,-1.));
#19213=DIRECTION('',(-0.707106781186547,0.707106781186548,8.65956056235494E-17));
#19214=DIRECTION('center_axis',(1.,0.,0.));
#19215=DIRECTION('ref_axis',(0.,1.,0.));
#19216=DIRECTION('center_axis',(1.,0.,0.));
#19217=DIRECTION('ref_axis',(0.,0.,-1.));
#19218=DIRECTION('',(-1.,0.,0.));
#19219=DIRECTION('center_axis',(-1.,0.,0.));
#19220=DIRECTION('ref_axis',(0.,1.,0.));
#19221=DIRECTION('center_axis',(1.,0.,0.));
#19222=DIRECTION('ref_axis',(0.,0.,-1.));
#19223=DIRECTION('',(-0.707106781186548,-0.707106781186548,-8.65956056235493E-17));
#19224=DIRECTION('center_axis',(1.,0.,0.));
#19225=DIRECTION('ref_axis',(0.,0.,-1.));
#19226=DIRECTION('center_axis',(1.,0.,0.));
#19227=DIRECTION('ref_axis',(0.,0.,-1.));
#19228=DIRECTION('center_axis',(1.,0.,0.));
#19229=DIRECTION('ref_axis',(0.,1.,0.));
#19230=DIRECTION('',(-0.961523947640823,0.274721127897378,3.36436349937675E-17));
#19231=DIRECTION('center_axis',(1.,0.,0.));
#19232=DIRECTION('ref_axis',(0.,0.,-1.));
#19233=DIRECTION('center_axis',(1.,0.,0.));
#19234=DIRECTION('ref_axis',(0.,0.,-1.));
#19235=DIRECTION('center_axis',(1.,0.,0.));
#19236=DIRECTION('ref_axis',(0.,0.,-1.));
#19237=DIRECTION('center_axis',(-1.,0.,0.));
#19238=DIRECTION('ref_axis',(0.,1.,0.));
#19239=DIRECTION('center_axis',(1.,0.,0.));
#19240=DIRECTION('ref_axis',(0.,0.,-1.));
#19241=DIRECTION('',(-0.919145030018057,-0.39391929857917,-4.82412008127351E-17));
#19242=DIRECTION('center_axis',(1.,0.,0.));
#19243=DIRECTION('ref_axis',(0.,0.,-1.));
#19244=DIRECTION('center_axis',(1.,0.,0.));
#19245=DIRECTION('ref_axis',(0.,0.,-1.));
#19246=DIRECTION('center_axis',(1.,0.,0.));
#19247=DIRECTION('ref_axis',(0.,1.,0.));
#19248=DIRECTION('',(-0.707106781186548,0.707106781186548,8.65956056235494E-17));
#19249=DIRECTION('center_axis',(1.,0.,0.));
#19250=DIRECTION('ref_axis',(0.,0.,-1.));
#19251=DIRECTION('center_axis',(1.,0.,0.));
#19252=DIRECTION('ref_axis',(0.,1.,0.));
#19253=DIRECTION('',(-1.,0.,0.));
#19254=DIRECTION('center_axis',(1.,0.,0.));
#19255=DIRECTION('ref_axis',(0.,0.,-1.));
#19256=DIRECTION('center_axis',(-1.,0.,0.));
#19257=DIRECTION('ref_axis',(0.,1.,0.));
#19258=DIRECTION('',(-0.707106781186547,-0.707106781186548,-8.65956056235494E-17));
#19259=DIRECTION('center_axis',(1.,0.,0.));
#19260=DIRECTION('ref_axis',(0.,0.,-1.));
#19261=DIRECTION('center_axis',(-1.,0.,0.));
#19262=DIRECTION('ref_axis',(0.,0.,1.));
#26845=CARTESIAN_POINT('',(0.,0.,0.));
#26846=CARTESIAN_POINT('Origin',(0.35,0.,0.));
#26847=CARTESIAN_POINT('',(0.7,-19.3,-2.36356832235439E-15));
#26848=CARTESIAN_POINT('Origin',(0.7,0.,0.));
#26849=CARTESIAN_POINT('',(-4.85722573273506E-16,-19.,-2.32682891837997E-15));
#26850=CARTESIAN_POINT('',(0.35,-19.15,-2.34519862036718E-15));
#26851=CARTESIAN_POINT('Origin',(0.,0.,0.));
#26852=CARTESIAN_POINT('Origin',(0.7,23.8,0.));
#26853=CARTESIAN_POINT('',(0.7,-23.8,-2.9146593819707E-15));
#26854=CARTESIAN_POINT('Origin',(0.7,0.,0.));
#26855=CARTESIAN_POINT('Origin',(0.35,0.,0.));
#26856=CARTESIAN_POINT('',(-1.04083408558608E-15,-24.,-2.93915231795365E-15));
#26857=CARTESIAN_POINT('',(0.35,-23.9,-2.92690584996217E-15));
#26858=CARTESIAN_POINT('Origin',(0.,0.,0.));
#26859=CARTESIAN_POINT('Origin',(0.,27.1,0.));
#26860=CARTESIAN_POINT('',(-4.85722573273506E-16,-27.1,-3.31879282568933E-15));
#26861=CARTESIAN_POINT('Origin',(0.,0.,0.));
#26862=CARTESIAN_POINT('Origin',(0.2,0.,0.));
#26863=CARTESIAN_POINT('',(0.4,-27.5,-3.36777869765522E-15));
#26864=CARTESIAN_POINT('Origin',(0.4,0.,0.));
#26865=CARTESIAN_POINT('',(0.2,-27.3,-3.34328576167227E-15));
#26866=CARTESIAN_POINT('Origin',(6.5,0.,0.));
#26867=CARTESIAN_POINT('',(12.6,-27.5,-3.36777869765522E-15));
#26868=CARTESIAN_POINT('Origin',(12.6,0.,0.));
#26869=CARTESIAN_POINT('',(6.5,-27.5,-3.36777869765522E-15));
#26870=CARTESIAN_POINT('Origin',(12.8,0.,0.));
#26871=CARTESIAN_POINT('',(13.,-27.1,-3.31879282568933E-15));
#26872=CARTESIAN_POINT('Origin',(13.,0.,0.));
#26873=CARTESIAN_POINT('',(12.8,-27.3,-3.34328576167227E-15));
#26874=CARTESIAN_POINT('Origin',(13.,24.,0.));
#26875=CARTESIAN_POINT('',(13.,-24.,-2.93915231795365E-15));
#26876=CARTESIAN_POINT('Origin',(13.,0.,0.));
#26877=CARTESIAN_POINT('Origin',(12.65,0.,0.));
#26878=CARTESIAN_POINT('',(12.3,-23.8,-2.9146593819707E-15));
#26879=CARTESIAN_POINT('',(12.65,-23.9,-2.92690584996217E-15));
#26880=CARTESIAN_POINT('Origin',(12.3,0.,0.));
#26881=CARTESIAN_POINT('Origin',(12.3,19.3,0.));
#26882=CARTESIAN_POINT('',(12.3,-19.3,-2.36356832235439E-15));
#26883=CARTESIAN_POINT('Origin',(12.3,0.,0.));
#26884=CARTESIAN_POINT('Origin',(12.65,0.,0.));
#26885=CARTESIAN_POINT('',(13.,-19.,-2.32682891837997E-15));
#26886=CARTESIAN_POINT('Origin',(13.,0.,0.));
#26887=CARTESIAN_POINT('',(12.65,-19.15,-2.34519862036718E-15));
#26888=CARTESIAN_POINT('Origin',(13.,15.4,0.));
#26889=CARTESIAN_POINT('',(13.,-15.4,-1.88595607068692E-15));
#26890=CARTESIAN_POINT('Origin',(13.,0.,0.));
#26891=CARTESIAN_POINT('Origin',(12.8,0.,0.));
#26892=CARTESIAN_POINT('',(12.6,-15.,-1.83697019872103E-15));
#26893=CARTESIAN_POINT('',(12.8,-15.2,-1.86146313470398E-15));
#26894=CARTESIAN_POINT('Origin',(12.6,0.,0.));
#26895=CARTESIAN_POINT('Origin',(6.5,0.,0.));
#26896=CARTESIAN_POINT('',(0.4,-15.,-1.83697019872103E-15));
#26897=CARTESIAN_POINT('',(6.5,-15.,-1.83697019872103E-15));
#26898=CARTESIAN_POINT('Origin',(0.4,0.,0.));
#26899=CARTESIAN_POINT('Origin',(0.2,0.,0.));
#26900=CARTESIAN_POINT('',(-2.42861286636753E-16,-15.4,-1.88595607068692E-15));
#26901=CARTESIAN_POINT('',(0.2,-15.2,-1.86146313470398E-15));
#26902=CARTESIAN_POINT('Origin',(0.,0.,0.));
#26903=CARTESIAN_POINT('Origin',(0.,19.,0.));
#38482=UNCERTAINTY_MEASURE_WITH_UNIT(LENGTH_MEASURE(0.01),#38508,
'DISTANCE_ACCURACY_VALUE',
'Maximum model space distance between geometric entities at asserted c
onnectivities');
#38490=UNCERTAINTY_MEASURE_WITH_UNIT(LENGTH_MEASURE(0.01),#38508,
'DISTANCE_ACCURACY_VALUE',
'Maximum model space distance between geometric entities at asserted c
onnectivities');
#38499=(
GEOMETRIC_REPRESENTATION_CONTEXT(3)
GLOBAL_UNCERTAINTY_ASSIGNED_CONTEXT((#38482))
GLOBAL_UNIT_ASSIGNED_CONTEXT((#38508,#38510,#38511))
REPRESENTATION_CONTEXT('','3D')
);
#38507=(
GEOMETRIC_REPRESENTATION_CONTEXT(3)
GLOBAL_UNCERTAINTY_ASSIGNED_CONTEXT((#38490))
GLOBAL_UNIT_ASSIGNED_CONTEXT((#38508,#38510,#38511))
REPRESENTATION_CONTEXT('','3D')
);
#38508=(
LENGTH_UNIT()
NAMED_UNIT(*)
SI_UNIT(.MILLI.,.METRE.)
);
#38510=(
NAMED_UNIT(*)
PLANE_ANGLE_UNIT()
SI_UNIT($,.RADIAN.)
);
#38511=(
NAMED_UNIT(*)
SI_UNIT($,.STERADIAN.)
SOLID_ANGLE_UNIT()
);
#38520=SHAPE_DEFINITION_REPRESENTATION(#38536,#38582);
#38536=PRODUCT_DEFINITION_SHAPE('',$,#38599);
#38582=SHAPE_REPRESENTATION('',(#16171),#38499);
#38590=PRODUCT_DEFINITION_CONTEXT('part definition',#38640,'design');
#38599=PRODUCT_DEFINITION('2026-10-26-01-10-54-631',
'11_Front_Bearing_6006',#38615,#38590);
#38615=PRODUCT_DEFINITION_FORMATION('',$,#38650);
#38640=APPLICATION_CONTEXT(
'Core Data for Automotive Mechanical Design Process');
#38641=PRODUCT_CONTEXT('part definition',#38640,'mechanical');
#38650=PRODUCT('2026-10-26-01-10-54-631','11_Front_Bearing_6006',$,(#38641));
#38714=COLOUR_RGB('Grey',0.48,0.52,0.57);
#38715=FILL_AREA_STYLE_COLOUR('',#38714);
#38716=FILL_AREA_STYLE('',(#38715));
#38717=SURFACE_STYLE_FILL_AREA(#38716);
#38718=SURFACE_SIDE_STYLE('',(#38717));
#38719=SURFACE_STYLE_USAGE(.BOTH.,#38718);
#38720=PRESENTATION_STYLE_ASSIGNMENT((#38719));
ENDSEC;
END-ISO-10303-21;
